ISO-10303-21;
HEADER;
/* Generated by software containing ST-Developer
 * from STEP Tools, Inc. (www.steptools.com) 
 */

FILE_DESCRIPTION(
/* description */ ('Four-bar parallelogram arm'),
/* implementation_level */ '2;1');

FILE_NAME(
/* name */ 'Bearing cap (7).step',
/* time_stamp */ '2026-10-28T03:24:55-07:00',
/* author */ (''),
/* organization */ (''),
/* preprocessor_version */ 'ST-DEVELOPER v20.2',
/* originating_system */ 'Autodesk Translation Framework v15.17.0.0',
/* authorisation */ '');

FILE_SCHEMA (('AUTOMOTIVE_DESIGN { 1 0 10303 214 3 1 1 }'));
ENDSEC;

DATA;
#10=MECHANICAL_DESIGN_GEOMETRIC_PRESENTATION_REPRESENTATION('',(#653),#14512);
#553=SHAPE_REPRESENTATION_RELATIONSHIP('SRR','None',#14776,#603);
#603=ADVANCED_BREP_SHAPE_REPRESENTATION('',(#710),#14491);
#653=STYLED_ITEM('',(#15087),#710);
#710=MANIFOLD_SOLID_BREP('Body1',#7358);
#927=FACE_BOUND('',#2071,.T.);
#928=FACE_BOUND('',#2072,.T.);
#929=FACE_BOUND('',#2073,.T.);
#930=FACE_BOUND('',#2074,.T.);
#931=FACE_BOUND('',#2075,.T.);
#932=FACE_BOUND('',#2077,.T.);
#933=FACE_BOUND('',#2078,.T.);
#934=FACE_BOUND('',#2079,.T.);
#935=FACE_BOUND('',#2080,.T.);
#936=FACE_BOUND('',#2081,.T.);
#1125=PLANE('',#8504);
#1126=PLANE('',#8505);
#1452=FACE_OUTER_BOUND('',#2064,.T.);
#1453=FACE_OUTER_BOUND('',#2065,.T.);
#1454=FACE_OUTER_BOUND('',#2066,.T.);
#1455=FACE_OUTER_BOUND('',#2067,.T.);
#1456=FACE_OUTER_BOUND('',#2068,.T.);
#1457=FACE_OUTER_BOUND('',#2069,.T.);
#1458=FACE_OUTER_BOUND('',#2070,.T.);
#1459=FACE_OUTER_BOUND('',#2076,.T.);
#2064=EDGE_LOOP('',(#6048,#6049,#6050,#6051));
#2065=EDGE_LOOP('',(#6052,#6053,#6054,#6055));
#2066=EDGE_LOOP('',(#6056,#6057,#6058,#6059));
#2067=EDGE_LOOP('',(#6060,#6061,#6062,#6063));
#2068=EDGE_LOOP('',(#6064,#6065,#6066,#6067));
#2069=EDGE_LOOP('',(#6068,#6069,#6070,#6071));
#2070=EDGE_LOOP('',(#6072));
#2071=EDGE_LOOP('',(#6073));
#2072=EDGE_LOOP('',(#6074));
#2073=EDGE_LOOP('',(#6075));
#2074=EDGE_LOOP('',(#6076));
#2075=EDGE_LOOP('',(#6077));
#2076=EDGE_LOOP('',(#6078));
#2077=EDGE_LOOP('',(#6079));
#2078=EDGE_LOOP('',(#6080));
#2079=EDGE_LOOP('',(#6081));
#2080=EDGE_LOOP('',(#6082));
#2081=EDGE_LOOP('',(#6083));
#2574=LINE('',#13202,#2968);
#2575=LINE('',#13208,#2969);
#2576=LINE('',#13214,#2970);
#2577=LINE('',#13220,#2971);
#2578=LINE('',#13226,#2972);
#2579=LINE('',#13232,#2973);
#2968=VECTOR('',#10332,0.225000000000001);
#2969=VECTOR('',#10339,0.225000000000001);
#2970=VECTOR('',#10346,0.225000000000001);
#2971=VECTOR('',#10353,0.225000000000001);
#2972=VECTOR('',#10360,1.02);
#2973=VECTOR('',#10367,2.2);
#3362=CIRCLE('',#8487,0.225000000000001);
#3363=CIRCLE('',#8488,0.225000000000001);
#3364=CIRCLE('',#8490,0.225000000000001);
#3365=CIRCLE('',#8491,0.225000000000001);
#3366=CIRCLE('',#8493,0.225000000000001);
#3367=CIRCLE('',#8494,0.225000000000001);
#3368=CIRCLE('',#8496,0.225000000000001);
#3369=CIRCLE('',#8497,0.225000000000001);
#3370=CIRCLE('',#8499,1.02);
#3371=CIRCLE('',#8500,1.02);
#3372=CIRCLE('',#8502,2.2);
#3373=CIRCLE('',#8503,2.2);
#3896=VERTEX_POINT('',#13199);
#3897=VERTEX_POINT('',#13201);
#3898=VERTEX_POINT('',#13205);
#3899=VERTEX_POINT('',#13207);
#3900=VERTEX_POINT('',#13211);
#3901=VERTEX_POINT('',#13213);
#3902=VERTEX_POINT('',#13217);
#3903=VERTEX_POINT('',#13219);
#3904=VERTEX_POINT('',#13223);
#3905=VERTEX_POINT('',#13225);
#3906=VERTEX_POINT('',#13229);
#3907=VERTEX_POINT('',#13231);
#4655=EDGE_CURVE('',#3896,#3896,#3362,.T.);
#4656=EDGE_CURVE('',#3896,#3897,#2574,.T.);
#4657=EDGE_CURVE('',#3897,#3897,#3363,.T.);
#4658=EDGE_CURVE('',#3898,#3898,#3364,.T.);
#4659=EDGE_CURVE('',#3898,#3899,#2575,.T.);
#4660=EDGE_CURVE('',#3899,#3899,#3365,.T.);
#4661=EDGE_CURVE('',#3900,#3900,#3366,.T.);
#4662=EDGE_CURVE('',#3900,#3901,#2576,.T.);
#4663=EDGE_CURVE('',#3901,#3901,#3367,.T.);
#4664=EDGE_CURVE('',#3902,#3902,#3368,.T.);
#4665=EDGE_CURVE('',#3902,#3903,#2577,.T.);
#4666=EDGE_CURVE('',#3903,#3903,#3369,.T.);
#4667=EDGE_CURVE('',#3904,#3904,#3370,.T.);
#4668=EDGE_CURVE('',#3904,#3905,#2578,.T.);
#4669=EDGE_CURVE('',#3905,#3905,#3371,.T.);
#4670=EDGE_CURVE('',#3906,#3906,#3372,.T.);
#4671=EDGE_CURVE('',#3906,#3907,#2579,.T.);
#4672=EDGE_CURVE('',#3907,#3907,#3373,.T.);
#6048=ORIENTED_EDGE('',*,*,#4655,.F.);
#6049=ORIENTED_EDGE('',*,*,#4656,.T.);
#6050=ORIENTED_EDGE('',*,*,#4657,.F.);
#6051=ORIENTED_EDGE('',*,*,#4656,.F.);
#6052=ORIENTED_EDGE('',*,*,#4658,.F.);
#6053=ORIENTED_EDGE('',*,*,#4659,.T.);
#6054=ORIENTED_EDGE('',*,*,#4660,.F.);
#6055=ORIENTED_EDGE('',*,*,#4659,.F.);
#6056=ORIENTED_EDGE('',*,*,#4661,.F.);
#6057=ORIENTED_EDGE('',*,*,#4662,.T.);
#6058=ORIENTED_EDGE('',*,*,#4663,.F.);
#6059=ORIENTED_EDGE('',*,*,#4662,.F.);
#6060=ORIENTED_EDGE('',*,*,#4664,.F.);
#6061=ORIENTED_EDGE('',*,*,#4665,.T.);
#6062=ORIENTED_EDGE('',*,*,#4666,.F.);
#6063=ORIENTED_EDGE('',*,*,#4665,.F.);
#6064=ORIENTED_EDGE('',*,*,#4667,.F.);
#6065=ORIENTED_EDGE('',*,*,#4668,.T.);
#6066=ORIENTED_EDGE('',*,*,#4669,.T.);
#6067=ORIENTED_EDGE('',*,*,#4668,.F.);
#6068=ORIENTED_EDGE('',*,*,#4670,.F.);
#6069=ORIENTED_EDGE('',*,*,#4671,.T.);
#6070=ORIENTED_EDGE('',*,*,#4672,.T.);
#6071=ORIENTED_EDGE('',*,*,#4671,.F.);
#6072=ORIENTED_EDGE('',*,*,#4670,.T.);
#6073=ORIENTED_EDGE('',*,*,#4667,.T.);
#6074=ORIENTED_EDGE('',*,*,#4666,.T.);
#6075=ORIENTED_EDGE('',*,*,#4663,.T.);
#6076=ORIENTED_EDGE('',*,*,#4660,.T.);
#6077=ORIENTED_EDGE('',*,*,#4657,.T.);
#6078=ORIENTED_EDGE('',*,*,#4672,.F.);
#6079=ORIENTED_EDGE('',*,*,#4669,.F.);
#6080=ORIENTED_EDGE('',*,*,#4664,.T.);
#6081=ORIENTED_EDGE('',*,*,#4661,.T.);
#6082=ORIENTED_EDGE('',*,*,#4658,.T.);
#6083=ORIENTED_EDGE('',*,*,#4655,.T.);
#6842=CYLINDRICAL_SURFACE('',#8486,0.225000000000001);
#6843=CYLINDRICAL_SURFACE('',#8489,0.225000000000001);
#6844=CYLINDRICAL_SURFACE('',#8492,0.225000000000001);
#6845=CYLINDRICAL_SURFACE('',#8495,0.225000000000001);
#6846=CYLINDRICAL_SURFACE('',#8498,1.02);
#6847=CYLINDRICAL_SURFACE('',#8501,2.2);
#7157=ADVANCED_FACE('',(#1452),#6842,.F.);
#7158=ADVANCED_FACE('',(#1453),#6843,.F.);
#7159=ADVANCED_FACE('',(#1454),#6844,.F.);
#7160=ADVANCED_FACE('',(#1455),#6845,.F.);
#7161=ADVANCED_FACE('',(#1456),#6846,.F.);
#7162=ADVANCED_FACE('',(#1457),#6847,.T.);
#7163=ADVANCED_FACE('',(#1458,#927,#928,#929,#930,#931),#1125,.T.);
#7164=ADVANCED_FACE('',(#1459,#932,#933,#934,#935,#936),#1126,.F.);
#7358=CLOSED_SHELL('',(#7157,#7158,#7159,#7160,#7161,#7162,#7163,#7164));
#8485=AXIS2_PLACEMENT_3D('',#13197,#10326,#10327);
#8486=AXIS2_PLACEMENT_3D('',#13198,#10328,#10329);
#8487=AXIS2_PLACEMENT_3D('',#13200,#10330,#10331);
#8488=AXIS2_PLACEMENT_3D('',#13203,#10333,#10334);
#8489=AXIS2_PLACEMENT_3D('',#13204,#10335,#10336);
#8490=AXIS2_PLACEMENT_3D('',#13206,#10337,#10338);
#8491=AXIS2_PLACEMENT_3D('',#13209,#10340,#10341);
#8492=AXIS2_PLACEMENT_3D('',#13210,#10342,#10343);
#8493=AXIS2_PLACEMENT_3D('',#13212,#10344,#10345);
#8494=AXIS2_PLACEMENT_3D('',#13215,#10347,#10348);
#8495=AXIS2_PLACEMENT_3D('',#13216,#10349,#10350);
#8496=AXIS2_PLACEMENT_3D('',#13218,#10351,#10352);
#8497=AXIS2_PLACEMENT_3D('',#13221,#10354,#10355);
#8498=AXIS2_PLACEMENT_3D('',#13222,#10356,#10357);
#8499=AXIS2_PLACEMENT_3D('',#13224,#10358,#10359);
#8500=AXIS2_PLACEMENT_3D('',#13227,#10361,#10362);
#8501=AXIS2_PLACEMENT_3D('',#13228,#10363,#10364);
#8502=AXIS2_PLACEMENT_3D('',#13230,#10365,#10366);
#8503=AXIS2_PLACEMENT_3D('',#13233,#10368,#10369);
#8504=AXIS2_PLACEMENT_3D('',#13234,#10370,#10371);
#8505=AXIS2_PLACEMENT_3D('',#13235,#10372,#10373);
#10326=DIRECTION('axis',(0.,0.,1.));
#10327=DIRECTION('refdir',(1.,0.,0.));
#10328=DIRECTION('center_axis',(0.,1.,0.));
#10329=DIRECTION('ref_axis',(1.,0.,0.));
#10330=DIRECTION('center_axis',(0.,1.,0.));
#10331=DIRECTION('ref_axis',(1.,0.,0.));
#10332=DIRECTION('',(0.,1.,0.));
#10333=DIRECTION('center_axis',(0.,-1.,0.));
#10334=DIRECTION('ref_axis',(1.,0.,0.));
#10335=DIRECTION('center_axis',(0.,1.,0.));
#10336=DIRECTION('ref_axis',(1.,0.,0.));
#10337=DIRECTION('center_axis',(0.,1.,0.));
#10338=DIRECTION('ref_axis',(1.,0.,0.));
#10339=DIRECTION('',(0.,1.,0.));
#10340=DIRECTION('center_axis',(0.,-1.,0.));
#10341=DIRECTION('ref_axis',(1.,0.,0.));
#10342=DIRECTION('center_axis',(0.,1.,0.));
#10343=DIRECTION('ref_axis',(1.,0.,0.));
#10344=DIRECTION('center_axis',(0.,1.,0.));
#10345=DIRECTION('ref_axis',(1.,0.,0.));
#10346=DIRECTION('',(0.,1.,0.));
#10347=DIRECTION('center_axis',(0.,-1.,0.));
#10348=DIRECTION('ref_axis',(1.,0.,0.));
#10349=DIRECTION('center_axis',(0.,1.,0.));
#10350=DIRECTION('ref_axis',(1.,0.,0.));
#10351=DIRECTION('center_axis',(0.,1.,0.));
#10352=DIRECTION('ref_axis',(1.,0.,0.));
#10353=DIRECTION('',(0.,1.,0.));
#10354=DIRECTION('center_axis',(0.,-1.,0.));
#10355=DIRECTION('ref_axis',(1.,0.,0.));
#10356=DIRECTION('center_axis',(0.,1.,0.));
#10357=DIRECTION('ref_axis',(1.,0.,0.));
#10358=DIRECTION('center_axis',(0.,-1.,0.));
#10359=DIRECTION('ref_axis',(1.,0.,0.));
#10360=DIRECTION('',(0.,-1.,0.));
#10361=DIRECTION('center_axis',(0.,-1.,0.));
#10362=DIRECTION('ref_axis',(1.,0.,0.));
#10363=DIRECTION('center_axis',(0.,1.,0.));
#10364=DIRECTION('ref_axis',(1.,0.,0.));
#10365=DIRECTION('center_axis',(0.,1.,0.));
#10366=DIRECTION('ref_axis',(1.,0.,0.));
#10367=DIRECTION('',(0.,-1.,0.));
#10368=DIRECTION('center_axis',(0.,1.,0.));
#10369=DIRECTION('ref_axis',(1.,0.,0.));
#10370=DIRECTION('center_axis',(0.,1.,0.));
#10371=DIRECTION('ref_axis',(1.,0.,0.));
#10372=DIRECTION('center_axis',(0.,1.,0.));
#10373=DIRECTION('ref_axis',(1.,0.,0.));
#13197=CARTESIAN_POINT('',(0.,0.,0.));
#13198=CARTESIAN_POINT('Origin',(18.7625631329235,0.95,12.7625631329235));
#13199=CARTESIAN_POINT('',(18.5375631329235,1.05,12.7625631329235));
#13200=CARTESIAN_POINT('Origin',(18.7625631329235,1.05,12.7625631329235));
#13201=CARTESIAN_POINT('',(18.5375631329235,1.4,12.7625631329235));
#13202=CARTESIAN_POINT('',(18.5375631329235,0.95,12.7625631329235));
#13203=CARTESIAN_POINT('Origin',(18.7625631329235,1.4,12.7625631329235));
#13204=CARTESIAN_POINT('Origin',(18.7625631329235,0.95,15.2374368670765));
#13205=CARTESIAN_POINT('',(18.5375631329235,1.05,15.2374368670765));
#13206=CARTESIAN_POINT('Origin',(18.7625631329235,1.05,15.2374368670765));
#13207=CARTESIAN_POINT('',(18.5375631329235,1.4,15.2374368670765));
#13208=CARTESIAN_POINT('',(18.5375631329235,0.95,15.2374368670765));
#13209=CARTESIAN_POINT('Origin',(18.7625631329235,1.4,15.2374368670765));
#13210=CARTESIAN_POINT('Origin',(21.2374368670765,0.95,15.2374368670765));
#13211=CARTESIAN_POINT('',(21.0124368670765,1.05,15.2374368670765));
#13212=CARTESIAN_POINT('Origin',(21.2374368670765,1.05,15.2374368670765));
#13213=CARTESIAN_POINT('',(21.0124368670765,1.4,15.2374368670765));
#13214=CARTESIAN_POINT('',(21.0124368670765,0.95,15.2374368670765));
#13215=CARTESIAN_POINT('Origin',(21.2374368670765,1.4,15.2374368670765));
#13216=CARTESIAN_POINT('Origin',(21.2374368670765,0.95,12.7625631329235));
#13217=CARTESIAN_POINT('',(21.0124368670765,1.05,12.7625631329235));
#13218=CARTESIAN_POINT('Origin',(21.2374368670765,1.05,12.7625631329235));
#13219=CARTESIAN_POINT('',(21.0124368670765,1.4,12.7625631329235));
#13220=CARTESIAN_POINT('',(21.0124368670765,0.95,12.7625631329235));
#13221=CARTESIAN_POINT('Origin',(21.2374368670765,1.4,12.7625631329235));
#13222=CARTESIAN_POINT('Origin',(20.,1.05,14.));
#13223=CARTESIAN_POINT('',(18.98,1.4,14.));
#13224=CARTESIAN_POINT('Origin',(20.,1.4,14.));
#13225=CARTESIAN_POINT('',(18.98,1.05,14.));
#13226=CARTESIAN_POINT('',(18.98,1.05,14.));
#13227=CARTESIAN_POINT('Origin',(20.,1.05,14.));
#13228=CARTESIAN_POINT('Origin',(20.,1.05,14.));
#13229=CARTESIAN_POINT('',(17.8,1.4,14.));
#13230=CARTESIAN_POINT('Origin',(20.,1.4,14.));
#13231=CARTESIAN_POINT('',(17.8,1.05,14.));
#13232=CARTESIAN_POINT('',(17.8,1.05,14.));
#13233=CARTESIAN_POINT('Origin',(20.,1.05,14.));
#13234=CARTESIAN_POINT('Origin',(20.,1.4,14.));
#13235=CARTESIAN_POINT('Origin',(20.,1.05,14.));
#14434=UNCERTAINTY_MEASURE_WITH_UNIT(LENGTH_MEASURE(0.001),#14513,
'DISTANCE_ACCURACY_VALUE',
'Maximum model space distance between geometric entities at asserted c
onnectivities');
#14455=UNCERTAINTY_MEASURE_WITH_UNIT(LENGTH_MEASURE(0.001),#14513,
'DISTANCE_ACCURACY_VALUE',
'Maximum model space distance between geometric entities at asserted c
onnectivities');
#14491=(
GEOMETRIC_REPRESENTATION_CONTEXT(3)
GLOBAL_UNCERTAINTY_ASSIGNED_CONTEXT((#14434))
GLOBAL_UNIT_ASSIGNED_CONTEXT((#14513,#14515,#14516))
REPRESENTATION_CONTEXT('','3D')
);
#14512=(
GEOMETRIC_REPRESENTATION_CONTEXT(3)
GLOBAL_UNCERTAINTY_ASSIGNED_CONTEXT((#14455))
GLOBAL_UNIT_ASSIGNED_CONTEXT((#14513,#14515,#14516))
REPRESENTATION_CONTEXT('','3D')
);
#14513=(
LENGTH_UNIT()
NAMED_UNIT(*)
SI_UNIT(.CENTI.,.METRE.)
);
#14515=(
NAMED_UNIT(*)
PLANE_ANGLE_UNIT()
SI_UNIT($,.RADIAN.)
);
#14516=(
NAMED_UNIT(*)
SI_UNIT($,.STERADIAN.)
SOLID_ANGLE_UNIT()
);
#14552=SHAPE_DEFINITION_REPRESENTATION(#14608,#14776);
#14608=PRODUCT_DEFINITION_SHAPE('',$,#14833);
#14776=SHAPE_REPRESENTATION('',(#8485),#14491);
#14797=PRODUCT_DEFINITION_CONTEXT('part definition',#14967,'design');
#14833=PRODUCT_DEFINITION('Bearing cap (7)','Bearing cap (7)',#14889,#14797);
#14889=PRODUCT_DEFINITION_FORMATION('',$,#15004);
#14967=APPLICATION_CONTEXT(
'Core Data for Automotive Mechanical Design Process');
#14968=PRODUCT_CONTEXT('part definition',#14967,'mechanical');
#15004=PRODUCT('Bearing cap (7)','Bearing cap (7)','Bearing cap (7)',(#14968));
#15081=COLOUR_RGB('Grey',0.48,0.52,0.57);
#15082=FILL_AREA_STYLE_COLOUR('',#15081);
#15083=FILL_AREA_STYLE('',(#15082));
#15084=SURFACE_STYLE_FILL_AREA(#15083);
#15085=SURFACE_SIDE_STYLE('',(#15084));
#15086=SURFACE_STYLE_USAGE(.BOTH.,#15085);
#15087=PRESENTATION_STYLE_ASSIGNMENT((#15086));
ENDSEC;
END-ISO-10303-21;
